ISO-10303-21;
HEADER;
/* Generated by software containing ST-Developer
 * from STEP Tools, Inc. (www.steptools.com) 
 */

FILE_DESCRIPTION(
/* description */ ('PAT-122'),
/* implementation_level */ '2;1');

FILE_NAME(
/* name */ 'Captive slot nut.step',
/* time_stamp */ '2026-10-29T20:20:12-07:00',
/* author */ (''),
/* organization */ (''),
/* preprocessor_version */ 'ST-DEVELOPER v20.2',
/* originating_system */ 'Autodesk Translation Framework v15.17.0.0',
/* authorisation */ '');

FILE_SCHEMA (('AUTOMOTIVE_DESIGN { 1 0 10303 214 3 1 1 }'));
ENDSEC;

DATA;
#10=MECHANICAL_DESIGN_GEOMETRIC_PRESENTATION_REPRESENTATION('',(#508),#10019);
#399=ELLIPSE('',#6247,0.299389011154384,0.2117);
#400=ELLIPSE('',#6251,0.299389011154384,0.2117);
#464=SHAPE_REPRESENTATION_RELATIONSHIP('SRR','None',#10185,#486);
#486=ADVANCED_BREP_SHAPE_REPRESENTATION('',(#528),#10014);
#508=STYLED_ITEM('',(#10355),#528);
#528=MANIFOLD_SOLID_BREP('Body1',#5632);
#602=FACE_BOUND('',#1426,.T.);
#786=PLANE('',#6237);
#787=PLANE('',#6238);
#788=PLANE('',#6239);
#789=PLANE('',#6241);
#790=PLANE('',#6242);
#791=PLANE('',#6243);
#792=PLANE('',#6244);
#793=PLANE('',#6245);
#794=PLANE('',#6246);
#795=PLANE('',#6253);
#796=PLANE('',#6254);
#797=PLANE('',#6255);
#798=PLANE('',#6256);
#1060=FACE_OUTER_BOUND('',#1423,.T.);
#1061=FACE_OUTER_BOUND('',#1424,.T.);
#1062=FACE_OUTER_BOUND('',#1425,.T.);
#1063=FACE_OUTER_BOUND('',#1427,.T.);
#1064=FACE_OUTER_BOUND('',#1428,.T.);
#1065=FACE_OUTER_BOUND('',#1429,.T.);
#1066=FACE_OUTER_BOUND('',#1430,.T.);
#1067=FACE_OUTER_BOUND('',#1431,.T.);
#1068=FACE_OUTER_BOUND('',#1432,.T.);
#1069=FACE_OUTER_BOUND('',#1433,.T.);
#1070=FACE_OUTER_BOUND('',#1434,.T.);
#1071=FACE_OUTER_BOUND('',#1435,.T.);
#1072=FACE_OUTER_BOUND('',#1436,.T.);
#1073=FACE_OUTER_BOUND('',#1437,.T.);
#1423=EDGE_LOOP('',(#5027,#5028,#5029,#5030));
#1424=EDGE_LOOP('',(#5031,#5032,#5033,#5034));
#1425=EDGE_LOOP('',(#5035,#5036,#5037,#5038));
#1426=EDGE_LOOP('',(#5039));
#1427=EDGE_LOOP('',(#5040,#5041,#5042,#5043,#5044,#5045,#5046,#5047,#5048,
#5049));
#1428=EDGE_LOOP('',(#5050,#5051,#5052,#5053));
#1429=EDGE_LOOP('',(#5054,#5055,#5056,#5057));
#1430=EDGE_LOOP('',(#5058,#5059,#5060,#5061,#5062,#5063,#5064,#5065,#5066,
#5067));
#1431=EDGE_LOOP('',(#5068,#5069,#5070,#5071));
#1432=EDGE_LOOP('',(#5072,#5073,#5074,#5075,#5076,#5077));
#1433=EDGE_LOOP('',(#5078,#5079,#5080,#5081,#5082,#5083,#5084,#5085));
#1434=EDGE_LOOP('',(#5086,#5087,#5088,#5089,#5090));
#1435=EDGE_LOOP('',(#5091,#5092,#5093,#5094));
#1436=EDGE_LOOP('',(#5095,#5096,#5097,#5098,#5099,#5100));
#1437=EDGE_LOOP('',(#5101,#5102,#5103,#5104));
#1945=LINE('',#9625,#2489);
#1946=LINE('',#9627,#2490);
#1947=LINE('',#9629,#2491);
#1948=LINE('',#9630,#2492);
#1949=LINE('',#9633,#2493);
#1950=LINE('',#9635,#2494);
#1951=LINE('',#9636,#2495);
#1952=LINE('',#9639,#2496);
#1953=LINE('',#9641,#2497);
#1954=LINE('',#9642,#2498);
#1955=LINE('',#9647,#2499);
#1956=LINE('',#9649,#2500);
#1957=LINE('',#9651,#2501);
#1958=LINE('',#9653,#2502);
#1959=LINE('',#9655,#2503);
#1960=LINE('',#9657,#2504);
#1961=LINE('',#9658,#2505);
#1962=LINE('',#9661,#2506);
#1963=LINE('',#9662,#2507);
#1964=LINE('',#9665,#2508);
#1965=LINE('',#9666,#2509);
#1966=LINE('',#9669,#2510);
#1967=LINE('',#9671,#2511);
#1968=LINE('',#9673,#2512);
#1969=LINE('',#9675,#2513);
#1970=LINE('',#9676,#2514);
#1971=LINE('',#9678,#2515);
#1972=LINE('',#9681,#2516);
#1973=LINE('',#9684,#2517);
#1974=LINE('',#9688,#2518);
#1975=LINE('',#9695,#2519);
#1976=LINE('',#9697,#2520);
#1977=LINE('',#9699,#2521);
#2489=VECTOR('',#7596,1.);
#2490=VECTOR('',#7597,1.);
#2491=VECTOR('',#7598,1.);
#2492=VECTOR('',#7599,1.);
#2493=VECTOR('',#7602,1.);
#2494=VECTOR('',#7603,1.);
#2495=VECTOR('',#7604,1.);
#2496=VECTOR('',#7607,1.);
#2497=VECTOR('',#7608,1.);
#2498=VECTOR('',#7609,1.);
#2499=VECTOR('',#7614,1.);
#2500=VECTOR('',#7615,1.);
#2501=VECTOR('',#7616,1.);
#2502=VECTOR('',#7617,1.);
#2503=VECTOR('',#7618,1.);
#2504=VECTOR('',#7619,1.);
#2505=VECTOR('',#7620,1.);
#2506=VECTOR('',#7623,1.);
#2507=VECTOR('',#7624,1.);
#2508=VECTOR('',#7627,1.);
#2509=VECTOR('',#7628,1.);
#2510=VECTOR('',#7631,1.);
#2511=VECTOR('',#7632,1.);
#2512=VECTOR('',#7633,1.);
#2513=VECTOR('',#7634,1.);
#2514=VECTOR('',#7635,1.);
#2515=VECTOR('',#7638,1.);
#2516=VECTOR('',#7641,1.);
#2517=VECTOR('',#7644,1.);
#2518=VECTOR('',#7649,0.21);
#2519=VECTOR('',#7658,1.);
#2520=VECTOR('',#7661,1.);
#2521=VECTOR('',#7664,1.);
#2676=CIRCLE('',#6240,0.2117);
#2677=CIRCLE('',#6249,0.2117);
#2678=CIRCLE('',#6250,0.2117);
#2679=CIRCLE('',#6252,0.2117);
#3092=VERTEX_POINT('',#9623);
#3093=VERTEX_POINT('',#9624);
#3094=VERTEX_POINT('',#9626);
#3095=VERTEX_POINT('',#9628);
#3096=VERTEX_POINT('',#9632);
#3097=VERTEX_POINT('',#9634);
#3098=VERTEX_POINT('',#9638);
#3099=VERTEX_POINT('',#9640);
#3100=VERTEX_POINT('',#9643);
#3101=VERTEX_POINT('',#9646);
#3102=VERTEX_POINT('',#9648);
#3103=VERTEX_POINT('',#9650);
#3104=VERTEX_POINT('',#9652);
#3105=VERTEX_POINT('',#9654);
#3106=VERTEX_POINT('',#9656);
#3107=VERTEX_POINT('',#9660);
#3108=VERTEX_POINT('',#9664);
#3109=VERTEX_POINT('',#9668);
#3110=VERTEX_POINT('',#9670);
#3111=VERTEX_POINT('',#9672);
#3112=VERTEX_POINT('',#9674);
#3113=VERTEX_POINT('',#9680);
#3114=VERTEX_POINT('',#9682);
#3115=VERTEX_POINT('',#9686);
#3116=VERTEX_POINT('',#9689);
#3117=VERTEX_POINT('',#9691);
#3748=EDGE_CURVE('',#3092,#3093,#1945,.T.);
#3749=EDGE_CURVE('',#3094,#3092,#1946,.T.);
#3750=EDGE_CURVE('',#3095,#3094,#1947,.T.);
#3751=EDGE_CURVE('',#3093,#3095,#1948,.T.);
#3752=EDGE_CURVE('',#3094,#3096,#1949,.T.);
#3753=EDGE_CURVE('',#3097,#3096,#1950,.T.);
#3754=EDGE_CURVE('',#3095,#3097,#1951,.T.);
#3755=EDGE_CURVE('',#3096,#3098,#1952,.T.);
#3756=EDGE_CURVE('',#3098,#3099,#1953,.T.);
#3757=EDGE_CURVE('',#3099,#3097,#1954,.T.);
#3758=EDGE_CURVE('',#3100,#3100,#2676,.T.);
#3759=EDGE_CURVE('',#3101,#3092,#1955,.T.);
#3760=EDGE_CURVE('',#3102,#3101,#1956,.T.);
#3761=EDGE_CURVE('',#3102,#3103,#1957,.T.);
#3762=EDGE_CURVE('',#3104,#3103,#1958,.T.);
#3763=EDGE_CURVE('',#3104,#3105,#1959,.T.);
#3764=EDGE_CURVE('',#3105,#3106,#1960,.T.);
#3765=EDGE_CURVE('',#3106,#3098,#1961,.T.);
#3766=EDGE_CURVE('',#3106,#3107,#1962,.T.);
#3767=EDGE_CURVE('',#3107,#3099,#1963,.T.);
#3768=EDGE_CURVE('',#3108,#3105,#1964,.T.);
#3769=EDGE_CURVE('',#3107,#3108,#1965,.T.);
#3770=EDGE_CURVE('',#3109,#3108,#1966,.T.);
#3771=EDGE_CURVE('',#3110,#3109,#1967,.T.);
#3772=EDGE_CURVE('',#3110,#3111,#1968,.T.);
#3773=EDGE_CURVE('',#3112,#3111,#1969,.T.);
#3774=EDGE_CURVE('',#3112,#3093,#1970,.T.);
#3775=EDGE_CURVE('',#3109,#3104,#1971,.T.);
#3776=EDGE_CURVE('',#3103,#3113,#1972,.T.);
#3777=EDGE_CURVE('',#3113,#3114,#399,.T.);
#3778=EDGE_CURVE('',#3114,#3110,#1973,.T.);
#3779=EDGE_CURVE('',#3115,#3113,#2677,.F.);
#3780=EDGE_CURVE('',#3115,#3100,#1974,.T.);
#3781=EDGE_CURVE('',#3116,#3115,#2678,.F.);
#3782=EDGE_CURVE('',#3117,#3116,#400,.T.);
#3783=EDGE_CURVE('',#3114,#3117,#2679,.F.);
#3784=EDGE_CURVE('',#3116,#3102,#1975,.T.);
#3785=EDGE_CURVE('',#3111,#3117,#1976,.T.);
#3786=EDGE_CURVE('',#3101,#3112,#1977,.T.);
#5027=ORIENTED_EDGE('',*,*,#3748,.F.);
#5028=ORIENTED_EDGE('',*,*,#3749,.F.);
#5029=ORIENTED_EDGE('',*,*,#3750,.F.);
#5030=ORIENTED_EDGE('',*,*,#3751,.F.);
#5031=ORIENTED_EDGE('',*,*,#3750,.T.);
#5032=ORIENTED_EDGE('',*,*,#3752,.T.);
#5033=ORIENTED_EDGE('',*,*,#3753,.F.);
#5034=ORIENTED_EDGE('',*,*,#3754,.F.);
#5035=ORIENTED_EDGE('',*,*,#3755,.T.);
#5036=ORIENTED_EDGE('',*,*,#3756,.T.);
#5037=ORIENTED_EDGE('',*,*,#3757,.T.);
#5038=ORIENTED_EDGE('',*,*,#3753,.T.);
#5039=ORIENTED_EDGE('',*,*,#3758,.T.);
#5040=ORIENTED_EDGE('',*,*,#3755,.F.);
#5041=ORIENTED_EDGE('',*,*,#3752,.F.);
#5042=ORIENTED_EDGE('',*,*,#3749,.T.);
#5043=ORIENTED_EDGE('',*,*,#3759,.F.);
#5044=ORIENTED_EDGE('',*,*,#3760,.F.);
#5045=ORIENTED_EDGE('',*,*,#3761,.T.);
#5046=ORIENTED_EDGE('',*,*,#3762,.F.);
#5047=ORIENTED_EDGE('',*,*,#3763,.T.);
#5048=ORIENTED_EDGE('',*,*,#3764,.T.);
#5049=ORIENTED_EDGE('',*,*,#3765,.T.);
#5050=ORIENTED_EDGE('',*,*,#3766,.T.);
#5051=ORIENTED_EDGE('',*,*,#3767,.T.);
#5052=ORIENTED_EDGE('',*,*,#3756,.F.);
#5053=ORIENTED_EDGE('',*,*,#3765,.F.);
#5054=ORIENTED_EDGE('',*,*,#3768,.F.);
#5055=ORIENTED_EDGE('',*,*,#3769,.F.);
#5056=ORIENTED_EDGE('',*,*,#3766,.F.);
#5057=ORIENTED_EDGE('',*,*,#3764,.F.);
#5058=ORIENTED_EDGE('',*,*,#3757,.F.);
#5059=ORIENTED_EDGE('',*,*,#3767,.F.);
#5060=ORIENTED_EDGE('',*,*,#3769,.T.);
#5061=ORIENTED_EDGE('',*,*,#3770,.F.);
#5062=ORIENTED_EDGE('',*,*,#3771,.F.);
#5063=ORIENTED_EDGE('',*,*,#3772,.T.);
#5064=ORIENTED_EDGE('',*,*,#3773,.F.);
#5065=ORIENTED_EDGE('',*,*,#3774,.T.);
#5066=ORIENTED_EDGE('',*,*,#3751,.T.);
#5067=ORIENTED_EDGE('',*,*,#3754,.T.);
#5068=ORIENTED_EDGE('',*,*,#3768,.T.);
#5069=ORIENTED_EDGE('',*,*,#3763,.F.);
#5070=ORIENTED_EDGE('',*,*,#3775,.F.);
#5071=ORIENTED_EDGE('',*,*,#3770,.T.);
#5072=ORIENTED_EDGE('',*,*,#3771,.T.);
#5073=ORIENTED_EDGE('',*,*,#3775,.T.);
#5074=ORIENTED_EDGE('',*,*,#3762,.T.);
#5075=ORIENTED_EDGE('',*,*,#3776,.T.);
#5076=ORIENTED_EDGE('',*,*,#3777,.T.);
#5077=ORIENTED_EDGE('',*,*,#3778,.T.);
#5078=ORIENTED_EDGE('',*,*,#3777,.F.);
#5079=ORIENTED_EDGE('',*,*,#3779,.F.);
#5080=ORIENTED_EDGE('',*,*,#3780,.T.);
#5081=ORIENTED_EDGE('',*,*,#3758,.F.);
#5082=ORIENTED_EDGE('',*,*,#3780,.F.);
#5083=ORIENTED_EDGE('',*,*,#3781,.F.);
#5084=ORIENTED_EDGE('',*,*,#3782,.F.);
#5085=ORIENTED_EDGE('',*,*,#3783,.F.);
#5086=ORIENTED_EDGE('',*,*,#3776,.F.);
#5087=ORIENTED_EDGE('',*,*,#3761,.F.);
#5088=ORIENTED_EDGE('',*,*,#3784,.F.);
#5089=ORIENTED_EDGE('',*,*,#3781,.T.);
#5090=ORIENTED_EDGE('',*,*,#3779,.T.);
#5091=ORIENTED_EDGE('',*,*,#3778,.F.);
#5092=ORIENTED_EDGE('',*,*,#3783,.T.);
#5093=ORIENTED_EDGE('',*,*,#3785,.F.);
#5094=ORIENTED_EDGE('',*,*,#3772,.F.);
#5095=ORIENTED_EDGE('',*,*,#3760,.T.);
#5096=ORIENTED_EDGE('',*,*,#3786,.T.);
#5097=ORIENTED_EDGE('',*,*,#3773,.T.);
#5098=ORIENTED_EDGE('',*,*,#3785,.T.);
#5099=ORIENTED_EDGE('',*,*,#3782,.T.);
#5100=ORIENTED_EDGE('',*,*,#3784,.T.);
#5101=ORIENTED_EDGE('',*,*,#3748,.T.);
#5102=ORIENTED_EDGE('',*,*,#3774,.F.);
#5103=ORIENTED_EDGE('',*,*,#3786,.F.);
#5104=ORIENTED_EDGE('',*,*,#3759,.T.);
#5312=CYLINDRICAL_SURFACE('',#6248,0.2117);
#5556=ADVANCED_FACE('',(#1060),#786,.F.);
#5557=ADVANCED_FACE('',(#1061),#787,.T.);
#5558=ADVANCED_FACE('',(#1062,#602),#788,.T.);
#5559=ADVANCED_FACE('',(#1063),#789,.T.);
#5560=ADVANCED_FACE('',(#1064),#790,.T.);
#5561=ADVANCED_FACE('',(#1065),#791,.F.);
#5562=ADVANCED_FACE('',(#1066),#792,.T.);
#5563=ADVANCED_FACE('',(#1067),#793,.T.);
#5564=ADVANCED_FACE('',(#1068),#794,.T.);
#5565=ADVANCED_FACE('',(#1069),#5312,.F.);
#5566=ADVANCED_FACE('',(#1070),#795,.F.);
#5567=ADVANCED_FACE('',(#1071),#796,.F.);
#5568=ADVANCED_FACE('',(#1072),#797,.T.);
#5569=ADVANCED_FACE('',(#1073),#798,.T.);
#5632=CLOSED_SHELL('',(#5556,#5557,#5558,#5559,#5560,#5561,#5562,#5563,
#5564,#5565,#5566,#5567,#5568,#5569));
#6236=AXIS2_PLACEMENT_3D('',#9621,#7592,#7593);
#6237=AXIS2_PLACEMENT_3D('',#9622,#7594,#7595);
#6238=AXIS2_PLACEMENT_3D('',#9631,#7600,#7601);
#6239=AXIS2_PLACEMENT_3D('',#9637,#7605,#7606);
#6240=AXIS2_PLACEMENT_3D('',#9644,#7610,#7611);
#6241=AXIS2_PLACEMENT_3D('',#9645,#7612,#7613);
#6242=AXIS2_PLACEMENT_3D('',#9659,#7621,#7622);
#6243=AXIS2_PLACEMENT_3D('',#9663,#7625,#7626);
#6244=AXIS2_PLACEMENT_3D('',#9667,#7629,#7630);
#6245=AXIS2_PLACEMENT_3D('',#9677,#7636,#7637);
#6246=AXIS2_PLACEMENT_3D('',#9679,#7639,#7640);
#6247=AXIS2_PLACEMENT_3D('',#9683,#7642,#7643);
#6248=AXIS2_PLACEMENT_3D('',#9685,#7645,#7646);
#6249=AXIS2_PLACEMENT_3D('',#9687,#7647,#7648);
#6250=AXIS2_PLACEMENT_3D('',#9690,#7650,#7651);
#6251=AXIS2_PLACEMENT_3D('',#9692,#7652,#7653);
#6252=AXIS2_PLACEMENT_3D('',#9693,#7654,#7655);
#6253=AXIS2_PLACEMENT_3D('',#9694,#7656,#7657);
#6254=AXIS2_PLACEMENT_3D('',#9696,#7659,#7660);
#6255=AXIS2_PLACEMENT_3D('',#9698,#7662,#7663);
#6256=AXIS2_PLACEMENT_3D('',#9700,#7665,#7666);
#7592=DIRECTION('axis',(0.,0.,1.));
#7593=DIRECTION('refdir',(1.,0.,0.));
#7594=DIRECTION('center_axis',(0.,0.,1.));
#7595=DIRECTION('ref_axis',(1.,0.,0.));
#7596=DIRECTION('',(1.,0.,0.));
#7597=DIRECTION('',(0.,-1.,0.));
#7598=DIRECTION('',(-1.,0.,0.));
#7599=DIRECTION('',(0.,1.,0.));
#7600=DIRECTION('center_axis',(0.,1.,0.));
#7601=DIRECTION('ref_axis',(-1.,0.,0.));
#7602=DIRECTION('',(0.,0.,1.));
#7603=DIRECTION('',(-1.,0.,0.));
#7604=DIRECTION('',(0.,0.,1.));
#7605=DIRECTION('center_axis',(0.,0.,1.));
#7606=DIRECTION('ref_axis',(1.,0.,0.));
#7607=DIRECTION('',(0.,-1.,0.));
#7608=DIRECTION('',(1.,0.,0.));
#7609=DIRECTION('',(0.,1.,0.));
#7610=DIRECTION('center_axis',(0.,0.,-1.));
#7611=DIRECTION('ref_axis',(1.,0.,0.));
#7612=DIRECTION('center_axis',(-1.,0.,0.));
#7613=DIRECTION('ref_axis',(0.,-1.,0.));
#7614=DIRECTION('',(0.,0.,1.));
#7615=DIRECTION('',(0.,0.707106781186548,0.707106781186548));
#7616=DIRECTION('',(0.,-1.,0.));
#7617=DIRECTION('',(0.,0.707106781186548,-0.707106781186548));
#7618=DIRECTION('',(0.,0.,1.));
#7619=DIRECTION('',(0.,-1.,0.));
#7620=DIRECTION('',(0.,0.,1.));
#7621=DIRECTION('center_axis',(0.,-1.,0.));
#7622=DIRECTION('ref_axis',(1.,0.,0.));
#7623=DIRECTION('',(1.,0.,0.));
#7624=DIRECTION('',(0.,0.,1.));
#7625=DIRECTION('center_axis',(0.,0.,1.));
#7626=DIRECTION('ref_axis',(1.,0.,0.));
#7627=DIRECTION('',(-1.,0.,0.));
#7628=DIRECTION('',(0.,1.,0.));
#7629=DIRECTION('center_axis',(1.,0.,0.));
#7630=DIRECTION('ref_axis',(0.,1.,0.));
#7631=DIRECTION('',(0.,0.,1.));
#7632=DIRECTION('',(0.,-0.707106781186548,0.707106781186548));
#7633=DIRECTION('',(0.,1.,0.));
#7634=DIRECTION('',(0.,-0.707106781186548,-0.707106781186548));
#7635=DIRECTION('',(0.,0.,1.));
#7636=DIRECTION('center_axis',(0.,-1.,0.));
#7637=DIRECTION('ref_axis',(1.,0.,0.));
#7638=DIRECTION('',(-1.,0.,0.));
#7639=DIRECTION('center_axis',(0.,-0.707106781186548,-0.707106781186548));
#7640=DIRECTION('ref_axis',(-1.,0.,0.));
#7641=DIRECTION('',(1.,0.,0.));
#7642=DIRECTION('center_axis',(0.,0.707106781186548,0.707106781186548));
#7643=DIRECTION('ref_axis',(0.,0.707106781186547,-0.707106781186547));
#7644=DIRECTION('',(1.,0.,0.));
#7645=DIRECTION('center_axis',(0.,0.,1.));
#7646=DIRECTION('ref_axis',(1.,0.,0.));
#7647=DIRECTION('center_axis',(0.,0.,-1.));
#7648=DIRECTION('ref_axis',(1.,0.,0.));
#7649=DIRECTION('',(0.,0.,1.));
#7650=DIRECTION('center_axis',(0.,0.,-1.));
#7651=DIRECTION('ref_axis',(1.,0.,0.));
#7652=DIRECTION('center_axis',(0.,-0.707106781186548,0.707106781186548));
#7653=DIRECTION('ref_axis',(0.,0.707106781186547,0.707106781186547));
#7654=DIRECTION('center_axis',(0.,0.,-1.));
#7655=DIRECTION('ref_axis',(1.,0.,0.));
#7656=DIRECTION('center_axis',(0.,0.,1.));
#7657=DIRECTION('ref_axis',(1.,0.,0.));
#7658=DIRECTION('',(-1.,0.,0.));
#7659=DIRECTION('center_axis',(0.,0.,1.));
#7660=DIRECTION('ref_axis',(1.,0.,0.));
#7661=DIRECTION('',(-1.,0.,0.));
#7662=DIRECTION('center_axis',(0.,0.707106781186548,-0.707106781186548));
#7663=DIRECTION('ref_axis',(-1.,0.,0.));
#7664=DIRECTION('',(1.,0.,0.));
#7665=DIRECTION('center_axis',(0.,1.,0.));
#7666=DIRECTION('ref_axis',(-1.,0.,0.));
#9621=CARTESIAN_POINT('',(0.,0.,0.));
#9622=CARTESIAN_POINT('Origin',(0.,0.395,0.25));
#9623=CARTESIAN_POINT('',(-0.5,0.3,0.25));
#9624=CARTESIAN_POINT('',(0.5,0.3,0.25));
#9625=CARTESIAN_POINT('',(0.25,0.3,0.25));
#9626=CARTESIAN_POINT('',(-0.5,0.5,0.25));
#9627=CARTESIAN_POINT('',(-0.5,0.5,0.25));
#9628=CARTESIAN_POINT('',(0.5,0.5,0.25));
#9629=CARTESIAN_POINT('',(0.5,0.5,0.25));
#9630=CARTESIAN_POINT('',(0.5,0.29,0.25));
#9631=CARTESIAN_POINT('Origin',(0.5,0.5,0.25));
#9632=CARTESIAN_POINT('',(-0.5,0.5,0.4));
#9633=CARTESIAN_POINT('',(-0.5,0.5,0.25));
#9634=CARTESIAN_POINT('',(0.5,0.5,0.4));
#9635=CARTESIAN_POINT('',(0.5,0.5,0.4));
#9636=CARTESIAN_POINT('',(0.5,0.5,0.25));
#9637=CARTESIAN_POINT('Origin',(0.,0.,0.4));
#9638=CARTESIAN_POINT('',(-0.5,-0.5,0.4));
#9639=CARTESIAN_POINT('',(-0.5,0.5,0.4));
#9640=CARTESIAN_POINT('',(0.5,-0.5,0.4));
#9641=CARTESIAN_POINT('',(-0.5,-0.5,0.4));
#9642=CARTESIAN_POINT('',(0.5,-0.3,0.4));
#9643=CARTESIAN_POINT('',(-0.2117,2.59257727379495E-17,0.4));
#9644=CARTESIAN_POINT('Origin',(0.,0.,0.4));
#9645=CARTESIAN_POINT('Origin',(-0.5,0.3,0.));
#9646=CARTESIAN_POINT('',(-0.5,0.3,0.15));
#9647=CARTESIAN_POINT('',(-0.5,0.3,0.));
#9648=CARTESIAN_POINT('',(-0.5,0.15,0.));
#9649=CARTESIAN_POINT('',(-0.5,0.225,0.075));
#9650=CARTESIAN_POINT('',(-0.5,-0.15,0.));
#9651=CARTESIAN_POINT('',(-0.5,0.3,0.));
#9652=CARTESIAN_POINT('',(-0.5,-0.3,0.15));
#9653=CARTESIAN_POINT('',(-0.5,-0.075,-0.075));
#9654=CARTESIAN_POINT('',(-0.5,-0.3,0.25));
#9655=CARTESIAN_POINT('',(-0.5,-0.3,0.));
#9656=CARTESIAN_POINT('',(-0.5,-0.5,0.25));
#9657=CARTESIAN_POINT('',(-0.5,-0.29,0.25));
#9658=CARTESIAN_POINT('',(-0.5,-0.5,0.25));
#9659=CARTESIAN_POINT('Origin',(-0.5,-0.5,0.25));
#9660=CARTESIAN_POINT('',(0.5,-0.5,0.25));
#9661=CARTESIAN_POINT('',(-0.5,-0.5,0.25));
#9662=CARTESIAN_POINT('',(0.5,-0.5,0.25));
#9663=CARTESIAN_POINT('Origin',(0.,-0.395,0.25));
#9664=CARTESIAN_POINT('',(0.5,-0.3,0.25));
#9665=CARTESIAN_POINT('',(-0.25,-0.3,0.25));
#9666=CARTESIAN_POINT('',(0.5,-0.5,0.25));
#9667=CARTESIAN_POINT('Origin',(0.5,-0.3,0.));
#9668=CARTESIAN_POINT('',(0.5,-0.3,0.15));
#9669=CARTESIAN_POINT('',(0.5,-0.3,0.));
#9670=CARTESIAN_POINT('',(0.5,-0.15,0.));
#9671=CARTESIAN_POINT('',(0.5,-0.225,0.075));
#9672=CARTESIAN_POINT('',(0.5,0.15,0.));
#9673=CARTESIAN_POINT('',(0.5,-0.3,0.));
#9674=CARTESIAN_POINT('',(0.5,0.3,0.15));
#9675=CARTESIAN_POINT('',(0.5,0.075,-0.075));
#9676=CARTESIAN_POINT('',(0.5,0.3,0.));
#9677=CARTESIAN_POINT('Origin',(-0.5,-0.3,0.));
#9678=CARTESIAN_POINT('',(-0.25,-0.3,0.15));
#9679=CARTESIAN_POINT('Origin',(-0.25,-0.225,0.075));
#9680=CARTESIAN_POINT('',(-0.149388386429468,-0.15,0.));
#9681=CARTESIAN_POINT('',(-0.25,-0.15,0.));
#9682=CARTESIAN_POINT('',(0.149388386429468,-0.15,0.));
#9683=CARTESIAN_POINT('Origin',(0.,0.,-0.15));
#9684=CARTESIAN_POINT('',(-0.25,-0.15,0.));
#9685=CARTESIAN_POINT('Origin',(0.,0.,-0.1));
#9686=CARTESIAN_POINT('',(-0.2117,-2.59257727379495E-17,0.));
#9687=CARTESIAN_POINT('Origin',(0.,0.,0.));
#9688=CARTESIAN_POINT('',(-0.2117,-2.59257727379495E-17,-0.1));
#9689=CARTESIAN_POINT('',(-0.149388386429468,0.15,0.));
#9690=CARTESIAN_POINT('Origin',(0.,0.,0.));
#9691=CARTESIAN_POINT('',(0.149388386429468,0.15,0.));
#9692=CARTESIAN_POINT('Origin',(0.,0.,-0.15));
#9693=CARTESIAN_POINT('Origin',(0.,0.,0.));
#9694=CARTESIAN_POINT('Origin',(0.,0.,0.));
#9695=CARTESIAN_POINT('',(0.25,0.15,0.));
#9696=CARTESIAN_POINT('Origin',(0.,0.,0.));
#9697=CARTESIAN_POINT('',(0.25,0.15,0.));
#9698=CARTESIAN_POINT('Origin',(0.25,0.225,0.075));
#9699=CARTESIAN_POINT('',(0.25,0.3,0.15));
#9700=CARTESIAN_POINT('Origin',(0.5,0.3,0.));
#9990=UNCERTAINTY_MEASURE_WITH_UNIT(LENGTH_MEASURE(0.001),#10020,
'DISTANCE_ACCURACY_VALUE',
'Maximum model space distance between geometric entities at asserted c
onnectivities');
#9995=UNCERTAINTY_MEASURE_WITH_UNIT(LENGTH_MEASURE(0.001),#10020,
'DISTANCE_ACCURACY_VALUE',
'Maximum model space distance between geometric entities at asserted c
onnectivities');
#10014=(
GEOMETRIC_REPRESENTATION_CONTEXT(3)
GLOBAL_UNCERTAINTY_ASSIGNED_CONTEXT((#9990))
GLOBAL_UNIT_ASSIGNED_CONTEXT((#10020,#10022,#10023))
REPRESENTATION_CONTEXT('','3D')
);
#10019=(
GEOMETRIC_REPRESENTATION_CONTEXT(3)
GLOBAL_UNCERTAINTY_ASSIGNED_CONTEXT((#9995))
GLOBAL_UNIT_ASSIGNED_CONTEXT((#10020,#10022,#10023))
REPRESENTATION_CONTEXT('','3D')
);
#10020=(
LENGTH_UNIT()
NAMED_UNIT(*)
SI_UNIT(.CENTI.,.METRE.)
);
#10022=(
NAMED_UNIT(*)
PLANE_ANGLE_UNIT()
SI_UNIT($,.RADIAN.)
);
#10023=(
NAMED_UNIT(*)
SI_UNIT($,.STERADIAN.)
SOLID_ANGLE_UNIT()
);
#10042=SHAPE_DEFINITION_REPRESENTATION(#10065,#10185);
#10065=PRODUCT_DEFINITION_SHAPE('',$,#10209);
#10185=SHAPE_REPRESENTATION('',(#6236),#10014);
#10190=PRODUCT_DEFINITION_CONTEXT('part definition',#10261,'design');
#10209=PRODUCT_DEFINITION('Captive slot nut','Captive slot nut',
#10232,#10190);
#10232=PRODUCT_DEFINITION_FORMATION('',$,#10281);
#10261=APPLICATION_CONTEXT(
'Core Data for Automotive Mechanical Design Process');
#10262=PRODUCT_CONTEXT('part definition',#10261,'mechanical');
#10281=PRODUCT('Captive slot nut','Captive slot nut',
'Captive slot nut',(#10262));
#10349=COLOUR_RGB('Black',0.12,0.14,0.17);
#10350=FILL_AREA_STYLE_COLOUR('',#10349);
#10351=FILL_AREA_STYLE('',(#10350));
#10352=SURFACE_STYLE_FILL_AREA(#10351);
#10353=SURFACE_SIDE_STYLE('',(#10352));
#10354=SURFACE_STYLE_USAGE(.BOTH.,#10353);
#10355=PRESENTATION_STYLE_ASSIGNMENT((#10354));
ENDSEC;
END-ISO-10303-21;
